ISO-10303-21;
HEADER;
/* Generated by software containing ST-Developer
 * from STEP Tools, Inc. (www.steptools.com) 
 */

FILE_DESCRIPTION(
/* description */ ('Jaw-coupled motor to shaft test stand'),
/* implementation_level */ '2;1');

FILE_NAME(
/* name */ 'Socket Set Screw - M4x6.step',
/* time_stamp */ '2026-10-27T10:46:06-07:00',
/* author */ (''),
/* organization */ (''),
/* preprocessor_version */ 'ST-DEVELOPER v20.2',
/* originating_system */ 'Autodesk Translation Framework v15.17.0.0',
/* authorisation */ '');

FILE_SCHEMA (('AUTOMOTIVE_DESIGN { 1 0 10303 214 3 1 1 }'));
ENDSEC;

DATA;
#10=MECHANICAL_DESIGN_GEOMETRIC_PRESENTATION_REPRESENTATION('',(#366),#19361);
#17=CONICAL_SURFACE('',#11856,0.185,0.785398163397449);
#18=CONICAL_SURFACE('',#11860,0.1625,0.785398163397449);
#301=SHAPE_REPRESENTATION_RELATIONSHIP('SRR','None',#19517,#333);
#333=ADVANCED_BREP_SHAPE_REPRESENTATION('',(#397),#19353);
#366=STYLED_ITEM('',(#19753),#397);
#397=MANIFOLD_SOLID_BREP('Body1',#11012);
#505=FACE_BOUND('',#2005,.T.);
#685=PLANE('',#11847);
#686=PLANE('',#11848);
#687=PLANE('',#11849);
#688=PLANE('',#11850);
#689=PLANE('',#11851);
#690=PLANE('',#11852);
#691=PLANE('',#11853);
#692=PLANE('',#11854);
#693=PLANE('',#11862);
#1275=FACE_OUTER_BOUND('',#1997,.T.);
#1276=FACE_OUTER_BOUND('',#1998,.T.);
#1277=FACE_OUTER_BOUND('',#1999,.T.);
#1278=FACE_OUTER_BOUND('',#2000,.T.);
#1279=FACE_OUTER_BOUND('',#2001,.T.);
#1280=FACE_OUTER_BOUND('',#2002,.T.);
#1281=FACE_OUTER_BOUND('',#2003,.T.);
#1282=FACE_OUTER_BOUND('',#2004,.T.);
#1283=FACE_OUTER_BOUND('',#2006,.T.);
#1284=FACE_OUTER_BOUND('',#2007,.T.);
#1285=FACE_OUTER_BOUND('',#2008,.T.);
#1286=FACE_OUTER_BOUND('',#2009,.T.);
#1997=EDGE_LOOP('',(#8424,#8425,#8426,#8427));
#1998=EDGE_LOOP('',(#8428,#8429,#8430,#8431));
#1999=EDGE_LOOP('',(#8432,#8433,#8434,#8435));
#2000=EDGE_LOOP('',(#8436,#8437,#8438,#8439));
#2001=EDGE_LOOP('',(#8440,#8441,#8442,#8443));
#2002=EDGE_LOOP('',(#8444,#8445,#8446,#8447));
#2003=EDGE_LOOP('',(#8448,#8449,#8450,#8451,#8452,#8453));
#2004=EDGE_LOOP('',(#8454));
#2005=EDGE_LOOP('',(#8455,#8456,#8457,#8458,#8459,#8460));
#2006=EDGE_LOOP('',(#8461,#8462,#8463,#8464));
#2007=EDGE_LOOP('',(#8465,#8466,#8467,#8468));
#2008=EDGE_LOOP('',(#8469,#8470,#8471,#8472));
#2009=EDGE_LOOP('',(#8473));
#2710=LINE('',#17261,#3863);
#2711=LINE('',#17263,#3864);
#2712=LINE('',#17265,#3865);
#2713=LINE('',#17266,#3866);
#2714=LINE('',#17269,#3867);
#2715=LINE('',#17271,#3868);
#2716=LINE('',#17272,#3869);
#2717=LINE('',#17275,#3870);
#2718=LINE('',#17277,#3871);
#2719=LINE('',#17278,#3872);
#2720=LINE('',#17281,#3873);
#2721=LINE('',#17283,#3874);
#2722=LINE('',#17284,#3875);
#2723=LINE('',#17287,#3876);
#2724=LINE('',#17289,#3877);
#2725=LINE('',#17290,#3878);
#2726=LINE('',#17292,#3879);
#2727=LINE('',#17293,#3880);
#2728=LINE('',#17301,#3881);
#2729=LINE('',#17305,#3882);
#2730=LINE('',#17309,#3883);
#3863=VECTOR('',#13625,1.);
#3864=VECTOR('',#13626,1.);
#3865=VECTOR('',#13627,1.);
#3866=VECTOR('',#13628,1.);
#3867=VECTOR('',#13631,1.);
#3868=VECTOR('',#13632,1.);
#3869=VECTOR('',#13633,1.);
#3870=VECTOR('',#13636,1.);
#3871=VECTOR('',#13637,1.);
#3872=VECTOR('',#13638,1.);
#3873=VECTOR('',#13641,1.);
#3874=VECTOR('',#13642,1.);
#3875=VECTOR('',#13643,1.);
#3876=VECTOR('',#13646,1.);
#3877=VECTOR('',#13647,1.);
#3878=VECTOR('',#13648,1.);
#3879=VECTOR('',#13651,1.);
#3880=VECTOR('',#13652,1.);
#3881=VECTOR('',#13663,0.185);
#3882=VECTOR('',#13668,0.2);
#3883=VECTOR('',#13673,0.1625);
#4845=CIRCLE('',#11855,0.17);
#4846=CIRCLE('',#11857,0.1954);
#4847=CIRCLE('',#11859,0.1954);
#4848=CIRCLE('',#11861,0.125);
#5309=VERTEX_POINT('',#17259);
#5310=VERTEX_POINT('',#17260);
#5311=VERTEX_POINT('',#17262);
#5312=VERTEX_POINT('',#17264);
#5313=VERTEX_POINT('',#17268);
#5314=VERTEX_POINT('',#17270);
#5315=VERTEX_POINT('',#17274);
#5316=VERTEX_POINT('',#17276);
#5317=VERTEX_POINT('',#17280);
#5318=VERTEX_POINT('',#17282);
#5319=VERTEX_POINT('',#17286);
#5320=VERTEX_POINT('',#17288);
#5321=VERTEX_POINT('',#17296);
#5322=VERTEX_POINT('',#17299);
#5323=VERTEX_POINT('',#17303);
#5324=VERTEX_POINT('',#17307);
#6423=EDGE_CURVE('',#5309,#5310,#2710,.T.);
#6424=EDGE_CURVE('',#5309,#5311,#2711,.T.);
#6425=EDGE_CURVE('',#5311,#5312,#2712,.T.);
#6426=EDGE_CURVE('',#5310,#5312,#2713,.T.);
#6427=EDGE_CURVE('',#5313,#5309,#2714,.T.);
#6428=EDGE_CURVE('',#5313,#5314,#2715,.T.);
#6429=EDGE_CURVE('',#5314,#5311,#2716,.T.);
#6430=EDGE_CURVE('',#5315,#5313,#2717,.T.);
#6431=EDGE_CURVE('',#5315,#5316,#2718,.T.);
#6432=EDGE_CURVE('',#5316,#5314,#2719,.T.);
#6433=EDGE_CURVE('',#5317,#5315,#2720,.T.);
#6434=EDGE_CURVE('',#5317,#5318,#2721,.T.);
#6435=EDGE_CURVE('',#5318,#5316,#2722,.T.);
#6436=EDGE_CURVE('',#5319,#5317,#2723,.T.);
#6437=EDGE_CURVE('',#5319,#5320,#2724,.T.);
#6438=EDGE_CURVE('',#5320,#5318,#2725,.T.);
#6439=EDGE_CURVE('',#5310,#5319,#2726,.T.);
#6440=EDGE_CURVE('',#5312,#5320,#2727,.T.);
#6441=EDGE_CURVE('',#5321,#5321,#4845,.T.);
#6442=EDGE_CURVE('',#5322,#5322,#4846,.T.);
#6443=EDGE_CURVE('',#5322,#5321,#2728,.T.);
#6444=EDGE_CURVE('',#5323,#5323,#4847,.F.);
#6445=EDGE_CURVE('',#5323,#5322,#2729,.T.);
#6446=EDGE_CURVE('',#5324,#5324,#4848,.T.);
#6447=EDGE_CURVE('',#5324,#5323,#2730,.T.);
#8424=ORIENTED_EDGE('',*,*,#6423,.F.);
#8425=ORIENTED_EDGE('',*,*,#6424,.T.);
#8426=ORIENTED_EDGE('',*,*,#6425,.T.);
#8427=ORIENTED_EDGE('',*,*,#6426,.F.);
#8428=ORIENTED_EDGE('',*,*,#6427,.F.);
#8429=ORIENTED_EDGE('',*,*,#6428,.T.);
#8430=ORIENTED_EDGE('',*,*,#6429,.T.);
#8431=ORIENTED_EDGE('',*,*,#6424,.F.);
#8432=ORIENTED_EDGE('',*,*,#6430,.F.);
#8433=ORIENTED_EDGE('',*,*,#6431,.T.);
#8434=ORIENTED_EDGE('',*,*,#6432,.T.);
#8435=ORIENTED_EDGE('',*,*,#6428,.F.);
#8436=ORIENTED_EDGE('',*,*,#6433,.F.);
#8437=ORIENTED_EDGE('',*,*,#6434,.T.);
#8438=ORIENTED_EDGE('',*,*,#6435,.T.);
#8439=ORIENTED_EDGE('',*,*,#6431,.F.);
#8440=ORIENTED_EDGE('',*,*,#6436,.F.);
#8441=ORIENTED_EDGE('',*,*,#6437,.T.);
#8442=ORIENTED_EDGE('',*,*,#6438,.T.);
#8443=ORIENTED_EDGE('',*,*,#6434,.F.);
#8444=ORIENTED_EDGE('',*,*,#6439,.F.);
#8445=ORIENTED_EDGE('',*,*,#6426,.T.);
#8446=ORIENTED_EDGE('',*,*,#6440,.T.);
#8447=ORIENTED_EDGE('',*,*,#6437,.F.);
#8448=ORIENTED_EDGE('',*,*,#6440,.F.);
#8449=ORIENTED_EDGE('',*,*,#6425,.F.);
#8450=ORIENTED_EDGE('',*,*,#6429,.F.);
#8451=ORIENTED_EDGE('',*,*,#6432,.F.);
#8452=ORIENTED_EDGE('',*,*,#6435,.F.);
#8453=ORIENTED_EDGE('',*,*,#6438,.F.);
#8454=ORIENTED_EDGE('',*,*,#6441,.F.);
#8455=ORIENTED_EDGE('',*,*,#6423,.T.);
#8456=ORIENTED_EDGE('',*,*,#6439,.T.);
#8457=ORIENTED_EDGE('',*,*,#6436,.T.);
#8458=ORIENTED_EDGE('',*,*,#6433,.T.);
#8459=ORIENTED_EDGE('',*,*,#6430,.T.);
#8460=ORIENTED_EDGE('',*,*,#6427,.T.);
#8461=ORIENTED_EDGE('',*,*,#6442,.F.);
#8462=ORIENTED_EDGE('',*,*,#6443,.T.);
#8463=ORIENTED_EDGE('',*,*,#6441,.T.);
#8464=ORIENTED_EDGE('',*,*,#6443,.F.);
#8465=ORIENTED_EDGE('',*,*,#6444,.F.);
#8466=ORIENTED_EDGE('',*,*,#6445,.T.);
#8467=ORIENTED_EDGE('',*,*,#6442,.T.);
#8468=ORIENTED_EDGE('',*,*,#6445,.F.);
#8469=ORIENTED_EDGE('',*,*,#6446,.F.);
#8470=ORIENTED_EDGE('',*,*,#6447,.T.);
#8471=ORIENTED_EDGE('',*,*,#6444,.T.);
#8472=ORIENTED_EDGE('',*,*,#6447,.F.);
#8473=ORIENTED_EDGE('',*,*,#6446,.T.);
#10346=CYLINDRICAL_SURFACE('',#11858,0.1954);
#10617=ADVANCED_FACE('',(#1275),#685,.F.);
#10618=ADVANCED_FACE('',(#1276),#686,.F.);
#10619=ADVANCED_FACE('',(#1277),#687,.F.);
#10620=ADVANCED_FACE('',(#1278),#688,.F.);
#10621=ADVANCED_FACE('',(#1279),#689,.F.);
#10622=ADVANCED_FACE('',(#1280),#690,.F.);
#10623=ADVANCED_FACE('',(#1281),#691,.F.);
#10624=ADVANCED_FACE('',(#1282,#505),#692,.T.);
#10625=ADVANCED_FACE('',(#1283),#17,.T.);
#10626=ADVANCED_FACE('',(#1284),#10346,.T.);
#10627=ADVANCED_FACE('',(#1285),#18,.T.);
#10628=ADVANCED_FACE('',(#1286),#693,.T.);
#11012=CLOSED_SHELL('',(#10617,#10618,#10619,#10620,#10621,#10622,#10623,
#10624,#10625,#10626,#10627,#10628));
#11846=AXIS2_PLACEMENT_3D('',#17257,#13621,#13622);
#11847=AXIS2_PLACEMENT_3D('',#17258,#13623,#13624);
#11848=AXIS2_PLACEMENT_3D('',#17267,#13629,#13630);
#11849=AXIS2_PLACEMENT_3D('',#17273,#13634,#13635);
#11850=AXIS2_PLACEMENT_3D('',#17279,#13639,#13640);
#11851=AXIS2_PLACEMENT_3D('',#17285,#13644,#13645);
#11852=AXIS2_PLACEMENT_3D('',#17291,#13649,#13650);
#11853=AXIS2_PLACEMENT_3D('',#17294,#13653,#13654);
#11854=AXIS2_PLACEMENT_3D('',#17295,#13655,#13656);
#11855=AXIS2_PLACEMENT_3D('',#17297,#13657,#13658);
#11856=AXIS2_PLACEMENT_3D('',#17298,#13659,#13660);
#11857=AXIS2_PLACEMENT_3D('',#17300,#13661,#13662);
#11858=AXIS2_PLACEMENT_3D('',#17302,#13664,#13665);
#11859=AXIS2_PLACEMENT_3D('',#17304,#13666,#13667);
#11860=AXIS2_PLACEMENT_3D('',#17306,#13669,#13670);
#11861=AXIS2_PLACEMENT_3D('',#17308,#13671,#13672);
#11862=AXIS2_PLACEMENT_3D('',#17310,#13674,#13675);
#13621=DIRECTION('axis',(0.,0.,1.));
#13622=DIRECTION('refdir',(1.,0.,0.));
#13623=DIRECTION('center_axis',(0.866025403784439,0.,-0.5));
#13624=DIRECTION('ref_axis',(0.5,0.,0.866025403784439));
#13625=DIRECTION('',(0.5,0.,0.866025403784439));
#13626=DIRECTION('',(0.,-1.,0.));
#13627=DIRECTION('',(0.5,0.,0.866025403784439));
#13628=DIRECTION('',(0.,-1.,0.));
#13629=DIRECTION('center_axis',(1.20185167898973E-16,0.,-1.));
#13630=DIRECTION('ref_axis',(1.,0.,1.20185167898973E-16));
#13631=DIRECTION('',(1.,0.,1.20185167898973E-16));
#13632=DIRECTION('',(0.,-1.,0.));
#13633=DIRECTION('',(1.,0.,1.20185167898973E-16));
#13634=DIRECTION('center_axis',(-0.866025403784439,0.,-0.5));
#13635=DIRECTION('ref_axis',(0.5,0.,-0.866025403784439));
#13636=DIRECTION('',(0.5,0.,-0.866025403784439));
#13637=DIRECTION('',(0.,-1.,0.));
#13638=DIRECTION('',(0.5,0.,-0.866025403784439));
#13639=DIRECTION('center_axis',(-0.866025403784439,0.,0.5));
#13640=DIRECTION('ref_axis',(-0.5,0.,-0.866025403784439));
#13641=DIRECTION('',(-0.5,0.,-0.866025403784439));
#13642=DIRECTION('',(0.,-1.,0.));
#13643=DIRECTION('',(-0.5,0.,-0.866025403784439));
#13644=DIRECTION('center_axis',(-2.40370335797945E-16,0.,1.));
#13645=DIRECTION('ref_axis',(-1.,0.,-2.40370335797945E-16));
#13646=DIRECTION('',(-1.,0.,-2.40370335797945E-16));
#13647=DIRECTION('',(0.,-1.,0.));
#13648=DIRECTION('',(-1.,0.,-2.40370335797945E-16));
#13649=DIRECTION('center_axis',(0.866025403784439,0.,0.5));
#13650=DIRECTION('ref_axis',(-0.5,0.,0.866025403784439));
#13651=DIRECTION('',(-0.5,0.,0.866025403784439));
#13652=DIRECTION('',(-0.5,0.,0.866025403784439));
#13653=DIRECTION('center_axis',(0.,-1.,0.));
#13654=DIRECTION('ref_axis',(0.,0.,-1.));
#13655=DIRECTION('center_axis',(0.,1.,0.));
#13656=DIRECTION('ref_axis',(0.,0.,1.));
#13657=DIRECTION('center_axis',(0.,-1.,0.));
#13658=DIRECTION('ref_axis',(1.,0.,0.));
#13659=DIRECTION('center_axis',(0.,-1.,0.));
#13660=DIRECTION('ref_axis',(1.,0.,0.));
#13661=DIRECTION('center_axis',(0.,-1.,0.));
#13662=DIRECTION('ref_axis',(1.,0.,0.));
#13663=DIRECTION('',(0.707106781186548,0.707106781186547,8.65956056235494E-17));
#13664=DIRECTION('center_axis',(0.,-1.,0.));
#13665=DIRECTION('ref_axis',(1.,0.,0.));
#13666=DIRECTION('center_axis',(0.,1.,0.));
#13667=DIRECTION('ref_axis',(1.,0.,0.));
#13668=DIRECTION('',(0.,1.,0.));
#13669=DIRECTION('center_axis',(0.,1.,0.));
#13670=DIRECTION('ref_axis',(1.,0.,0.));
#13671=DIRECTION('center_axis',(0.,-1.,0.));
#13672=DIRECTION('ref_axis',(1.,0.,0.));
#13673=DIRECTION('',(-0.707106781186548,0.707106781186547,-8.65956056235494E-17));
#13674=DIRECTION('center_axis',(0.,-1.,0.));
#13675=DIRECTION('ref_axis',(0.,0.,-1.));
#17257=CARTESIAN_POINT('',(0.,0.,0.));
#17258=CARTESIAN_POINT('Origin',(0.0577350269189626,0.,-0.1));
#17259=CARTESIAN_POINT('',(0.0577350269189626,0.,-0.1));
#17260=CARTESIAN_POINT('',(0.115470053837925,0.,0.));
#17261=CARTESIAN_POINT('',(0.0934187836487032,0.,-0.0381939203391614));
#17262=CARTESIAN_POINT('',(0.0577350269189626,-0.2,-0.1));
#17263=CARTESIAN_POINT('',(0.0577350269189626,0.,-0.1));
#17264=CARTESIAN_POINT('',(0.115470053837925,-0.2,0.));
#17265=CARTESIAN_POINT('',(0.115470053837925,-0.2,0.));
#17266=CARTESIAN_POINT('',(0.115470053837925,0.,0.));
#17267=CARTESIAN_POINT('Origin',(-0.0577350269189626,0.,-0.1));
#17268=CARTESIAN_POINT('',(-0.0577350269189626,0.,-0.1));
#17269=CARTESIAN_POINT('',(0.0561324865405187,0.,-0.1));
#17270=CARTESIAN_POINT('',(-0.0577350269189626,-0.2,-0.1));
#17271=CARTESIAN_POINT('',(-0.0577350269189626,0.,-0.1));
#17272=CARTESIAN_POINT('',(0.0577350269189626,-0.2,-0.1));
#17273=CARTESIAN_POINT('Origin',(-0.115470053837925,0.,-1.38777878078145E-17));
#17274=CARTESIAN_POINT('',(-0.115470053837925,0.,-1.41410031829988E-17));
#17275=CARTESIAN_POINT('',(-0.0797862971081845,0.,-0.0618060796608387));
#17276=CARTESIAN_POINT('',(-0.115470053837925,-0.2,-1.38777878078145E-17));
#17277=CARTESIAN_POINT('',(-0.115470053837925,0.,-1.41410031829988E-17));
#17278=CARTESIAN_POINT('',(-0.0577350269189626,-0.2,-0.1));
#17279=CARTESIAN_POINT('Origin',(-0.0577350269189626,0.,0.1));
#17280=CARTESIAN_POINT('',(-0.0577350269189626,0.,0.1));
#17281=CARTESIAN_POINT('',(-0.0509187836487033,0.,0.111806079660839));
#17282=CARTESIAN_POINT('',(-0.0577350269189626,-0.2,0.1));
#17283=CARTESIAN_POINT('',(-0.0577350269189626,0.,0.1));
#17284=CARTESIAN_POINT('',(-0.115470053837925,-0.2,-1.41410031829988E-17));
#17285=CARTESIAN_POINT('Origin',(0.0577350269189626,0.,0.1));
#17286=CARTESIAN_POINT('',(0.0577350269189626,0.,0.1));
#17287=CARTESIAN_POINT('',(0.113867513459481,0.,0.1));
#17288=CARTESIAN_POINT('',(0.0577350269189626,-0.2,0.1));
#17289=CARTESIAN_POINT('',(0.0577350269189626,0.,0.1));
#17290=CARTESIAN_POINT('',(-0.0577350269189626,-0.2,0.1));
#17291=CARTESIAN_POINT('Origin',(0.115470053837925,0.,0.));
#17292=CARTESIAN_POINT('',(0.122286297108185,0.,-0.0118060796608386));
#17293=CARTESIAN_POINT('',(0.0577350269189626,-0.2,0.1));
#17294=CARTESIAN_POINT('Origin',(0.,-0.2,0.));
#17295=CARTESIAN_POINT('Origin',(0.17,0.,0.));
#17296=CARTESIAN_POINT('',(-0.17,-8.67361737988404E-18,-2.0818995585505E-17));
#17297=CARTESIAN_POINT('Origin',(0.,0.,0.));
#17298=CARTESIAN_POINT('Origin',(0.,-0.015,0.));
#17299=CARTESIAN_POINT('',(-0.1954,-0.0254,-2.39295984553393E-17));
#17300=CARTESIAN_POINT('Origin',(0.,-0.0254,0.));
#17301=CARTESIAN_POINT('',(-0.185,-0.015,-2.2655965784226E-17));
#17302=CARTESIAN_POINT('Origin',(0.,-0.2775,0.));
#17303=CARTESIAN_POINT('',(-0.1954,-0.5296,2.39295984553393E-17));
#17304=CARTESIAN_POINT('Origin',(0.,-0.5296,0.));
#17305=CARTESIAN_POINT('',(-0.1954,-0.2775,-2.39295984553393E-17));
#17306=CARTESIAN_POINT('Origin',(0.,-0.5625,0.));
#17307=CARTESIAN_POINT('',(-0.125,-0.6,-1.53080849893419E-17));
#17308=CARTESIAN_POINT('Origin',(0.,-0.6,0.));
#17309=CARTESIAN_POINT('',(-0.1625,-0.5625,-1.99005104861445E-17));
#17310=CARTESIAN_POINT('Origin',(0.,-0.6,0.));
#19315=UNCERTAINTY_MEASURE_WITH_UNIT(LENGTH_MEASURE(0.001),#19362,
'DISTANCE_ACCURACY_VALUE',
'Maximum model space distance between geometric entities at asserted c
onnectivities');
#19323=UNCERTAINTY_MEASURE_WITH_UNIT(LENGTH_MEASURE(0.001),#19362,
'DISTANCE_ACCURACY_VALUE',
'Maximum model space distance between geometric entities at asserted c
onnectivities');
#19353=(
GEOMETRIC_REPRESENTATION_CONTEXT(3)
GLOBAL_UNCERTAINTY_ASSIGNED_CONTEXT((#19315))
GLOBAL_UNIT_ASSIGNED_CONTEXT((#19362,#19364,#19365))
REPRESENTATION_CONTEXT('','3D')
);
#19361=(
GEOMETRIC_REPRESENTATION_CONTEXT(3)
GLOBAL_UNCERTAINTY_ASSIGNED_CONTEXT((#19323))
GLOBAL_UNIT_ASSIGNED_CONTEXT((#19362,#19364,#19365))
REPRESENTATION_CONTEXT('','3D')
);
#19362=(
LENGTH_UNIT()
NAMED_UNIT(*)
SI_UNIT(.CENTI.,.METRE.)
);
#19364=(
NAMED_UNIT(*)
PLANE_ANGLE_UNIT()
SI_UNIT($,.RADIAN.)
);
#19365=(
NAMED_UNIT(*)
SI_UNIT($,.STERADIAN.)
SOLID_ANGLE_UNIT()
);
#19395=SHAPE_DEFINITION_REPRESENTATION(#19459,#19517);
#19459=PRODUCT_DEFINITION_SHAPE('',$,#19555);
#19517=SHAPE_REPRESENTATION('',(#11846),#19353);
#19525=PRODUCT_DEFINITION_CONTEXT('part definition',#19638,'design');
#19555=PRODUCT_DEFINITION('Socket Set Screw - M4x6',
'Socket Set Screw - M4x6',#19592,#19525);
#19592=PRODUCT_DEFINITION_FORMATION('',$,#19669);
#19638=APPLICATION_CONTEXT(
'Core Data for Automotive Mechanical Design Process');
#19639=PRODUCT_CONTEXT('part definition',#19638,'mechanical');
#19669=PRODUCT('Socket Set Screw - M4x6','Socket Set Screw - M4x6',
'Socket Set Screw - M4x6',(#19639));
#19747=COLOUR_RGB('Black',0.12,0.14,0.17);
#19748=FILL_AREA_STYLE_COLOUR('',#19747);
#19749=FILL_AREA_STYLE('',(#19748));
#19750=SURFACE_STYLE_FILL_AREA(#19749);
#19751=SURFACE_SIDE_STYLE('',(#19750));
#19752=SURFACE_STYLE_USAGE(.BOTH.,#19751);
#19753=PRESENTATION_STYLE_ASSIGNMENT((#19752));
ENDSEC;
END-ISO-10303-21;
